ISO-10303-21;
HEADER;
FILE_DESCRIPTION (('STEP AP214'),
    '1' );
FILE_NAME ('Base Pivot Pin.step',
    '2026-10-06T10:23:46',
    ( '' ),
    ( '' ),
    'SwSTEP 2.0',
    'SolidWorks 2020',
    '' );
FILE_SCHEMA (( 'AUTOMOTIVE_DESIGN' ));
ENDSEC;

DATA;
#6=DIRECTION ( 'NONE',  ( 0.000000000000000000, 0.9992330079037401447, -0.03915859951075795903 ) ) ;
#73=AXIS2_PLACEMENT_3D ( 'NONE', #20617, #20868, #18556 ) ;
#138=MECHANICAL_DESIGN_GEOMETRIC_PRESENTATION_REPRESENTATION('',(#5078),#1784);
#642=AXIS2_PLACEMENT_3D ( 'NONE', #14194, #22039, #12393 ) ;
#883=CYLINDRICAL_SURFACE ( 'NONE', #73, 1.499999999999999778 ) ;
#969=CARTESIAN_POINT ( 'NONE',  ( 28.84183937708599998, -36.05761098950961241, 70.36375082663613512 ) ) ;
#1012=EDGE_LOOP ( 'NONE', ( #18298, #22187, #18869, #14295 ) ) ;
#1121=VECTOR ( 'NONE', #18914, 1000.000000000000000 ) ;
#1128=CARTESIAN_POINT ( 'NONE',  ( 47.84183937708599643, -36.05761098950961241, 70.36375082663613512 ) ) ;
#1299=CARTESIAN_POINT ( 'NONE',  ( 28.84183937708599998, -33.05991196579839198, 70.24627502810386659 ) ) ;
#1713=APPLICATION_CONTEXT ( 'automotive_design' ) ;
#1784=( GEOMETRIC_REPRESENTATION_CONTEXT ( 3 ) GLOBAL_UNCERTAINTY_ASSIGNED_CONTEXT ( ( #24188 ) ) GLOBAL_UNIT_ASSIGNED_CONTEXT ( ( #11078, #5403, #24948 ) ) REPRESENTATION_CONTEXT ( 'NONE', 'WORKASPACE' ) );
#2000=AXIS2_PLACEMENT_3D ( 'NONE', #9286, #12766, #22537 ) ;
#2881=CARTESIAN_POINT ( 'NONE',  ( 47.84183937708599643, -34.55876147765400219, 70.30501292737000085 ) ) ;
#3230=COLOUR_RGB ( '', 0.09019608, 0.27058824, 0.51372549) ;
#3333=( LENGTH_UNIT ( ) NAMED_UNIT ( * ) SI_UNIT ( .MILLI., .METRE. ) );
#3441=COLOUR_RGB ( '', 0.09019608, 0.27058824, 0.51372549) ;
#3617=CARTESIAN_POINT ( 'NONE',  ( 47.84183937708599643, -34.55876147765400219, 70.30501292737000085 ) ) ;
#3843=SHAPE_REPRESENTATION_RELATIONSHIP ( 'NONE' , 'NONE' ,  #4169, #10468 ) ;
#4169=SHAPE_REPRESENTATION ( 'Base Pivot Pin', ( #2000 ), #6728 ) ;
#4213=DIRECTION ( 'NONE',  ( 1.000000000000000000, 0.000000000000000000, 0.000000000000000000 ) ) ;
#4639=( NAMED_UNIT ( * ) SI_UNIT ( $, .STERADIAN. ) SOLID_ANGLE_UNIT ( ) );
#4880=VERTEX_POINT ( 'NONE', #1299 ) ;
#5045=EDGE_LOOP ( 'NONE', ( #7807, #23486, #23253, #13343 ) ) ;
#5078=STYLED_ITEM ( 'NONE', ( #22792 ), #10468 ) ;
#5094=FACE_OUTER_BOUND ( 'NONE', #9055, .T. ) ;
#5101=EDGE_CURVE ( 'NONE', #22885, #4880, #15222, .T. ) ;
#5403=( NAMED_UNIT ( * ) PLANE_ANGLE_UNIT ( ) SI_UNIT ( $, .RADIAN. ) );
#5671=VERTEX_POINT ( 'NONE', #19657 ) ;
#6114=AXIS2_PLACEMENT_3D ( 'NONE', #2881, #24138, #18493 ) ;
#6309=VECTOR ( 'NONE', #20816, 1000.000000000000000 ) ;
#6371=PRODUCT_DEFINITION_FORMATION_WITH_SPECIFIED_SOURCE ( 'ANY', '', #23697, .NOT_KNOWN. ) ;
#6683=AXIS2_PLACEMENT_3D ( 'NONE', #24808, #7054, #22889 ) ;
#6700=PLANE ( 'NONE',  #642 ) ;
#6728=( GEOMETRIC_REPRESENTATION_CONTEXT ( 3 ) GLOBAL_UNCERTAINTY_ASSIGNED_CONTEXT ( ( #8504 ) ) GLOBAL_UNIT_ASSIGNED_CONTEXT ( ( #3333, #18933, #7076 ) ) REPRESENTATION_CONTEXT ( 'NONE', 'WORKASPACE' ) );
#6801=FACE_OUTER_BOUND ( 'NONE', #5045, .T. ) ;
#7054=DIRECTION ( 'NONE',  ( -1.000000000000000000, 0.000000000000000000, 0.000000000000000000 ) ) ;
#7060=LINE ( 'NONE', #14537, #1121 ) ;
#7076=( NAMED_UNIT ( * ) SI_UNIT ( $, .STERADIAN. ) SOLID_ANGLE_UNIT ( ) );
#7355=ORIENTED_EDGE ( 'NONE', *, *, #17843, .T. ) ;
#7395=ADVANCED_FACE ( 'NONE', ( #6801 ), #15034, .T. ) ;
#7807=ORIENTED_EDGE ( 'NONE', *, *, #18261, .F. ) ;
#7856=EDGE_CURVE ( 'NONE', #23981, #5671, #22296, .T. ) ;
#8504=UNCERTAINTY_MEASURE_WITH_UNIT (LENGTH_MEASURE( 1.000000000000000082E-05 ), #3333, 'distance_accuracy_value', 'NONE');
#8589=LINE ( 'NONE', #11023, #6309 ) ;
#8739=AXIS2_PLACEMENT_3D ( 'NONE', #13109, #22499, #16835 ) ;
#8932=EDGE_LOOP ( 'NONE', ( #15408, #19778 ) ) ;
#9024=FILL_AREA_STYLE ('',( #15054 ) ) ;
#9055=EDGE_LOOP ( 'NONE', ( #15941, #7355 ) ) ;
#9135=ADVANCED_FACE ( 'NONE', ( #10579 ), #6700, .F. ) ;
#9286=CARTESIAN_POINT ( 'NONE',  ( 0.000000000000000000, 0.000000000000000000, 0.000000000000000000 ) ) ;
#9847=PRESENTATION_STYLE_ASSIGNMENT (( #20224 ) ) ;
#10136=EDGE_CURVE ( 'NONE', #4880, #22885, #24374, .T. ) ;
#10334=EDGE_CURVE ( 'NONE', #23981, #22885, #8589, .T. ) ;
#10468=ADVANCED_BREP_SHAPE_REPRESENTATION ( '', ( #25444, #2000 ), #6728 ) ;
#10579=FACE_OUTER_BOUND ( 'NONE', #8932, .T. ) ;
#11023=CARTESIAN_POINT ( 'NONE',  ( 47.84183937708599643, -36.05761098950961241, 70.36375082663613512 ) ) ;
#11078=( LENGTH_UNIT ( ) NAMED_UNIT ( * ) SI_UNIT ( .MILLI., .METRE. ) );
#11209=SURFACE_SIDE_STYLE ('',( #16605 ) ) ;
#11493=CARTESIAN_POINT ( 'NONE',  ( 28.84183937708599998, -34.55876147765400219, 70.30501292737000085 ) ) ;
#12385=( LENGTH_UNIT ( ) NAMED_UNIT ( * ) SI_UNIT ( .MILLI., .METRE. ) );
#12393=DIRECTION ( 'NONE',  ( 0.000000000000000000, 0.9992330079037401447, -0.03915859951076000600 ) ) ;
#12766=DIRECTION ( 'NONE',  ( 0.000000000000000000, 0.000000000000000000, 1.000000000000000000 ) ) ;
#13109=CARTESIAN_POINT ( 'NONE',  ( 47.84183937708599643, -34.55876147765400219, 70.30501292737000085 ) ) ;
#13259=CIRCLE ( 'NONE', #8739, 1.499999999999999778 ) ;
#13343=ORIENTED_EDGE ( 'NONE', *, *, #5101, .T. ) ;
#13630=PRODUCT_DEFINITION_SHAPE ( 'NONE', 'NONE',  #17663 ) ;
#13802=DIRECTION ( 'NONE',  ( 1.000000000000000000, 0.000000000000000000, 0.000000000000000000 ) ) ;
#13831=SURFACE_SIDE_STYLE ('',( #14551 ) ) ;
#14194=CARTESIAN_POINT ( 'NONE',  ( 28.84183937708599998, -34.55876147765400219, 70.30501292737000085 ) ) ;
#14295=ORIENTED_EDGE ( 'NONE', *, *, #10334, .F. ) ;
#14393=PRODUCT_DEFINITION_CONTEXT ( 'detailed design', #1713, 'design' ) ;
#14428=( NAMED_UNIT ( * ) PLANE_ANGLE_UNIT ( ) SI_UNIT ( $, .RADIAN. ) );
#14537=CARTESIAN_POINT ( 'NONE',  ( 47.84183937708599643, -33.05991196579839198, 70.24627502810386659 ) ) ;
#14551=SURFACE_STYLE_FILL_AREA ( #16231 ) ;
#15034=CYLINDRICAL_SURFACE ( 'NONE', #6683, 1.499999999999999778 ) ;
#15054=FILL_AREA_STYLE_COLOUR ( '', #3441 ) ;
#15222=CIRCLE ( 'NONE', #16053, 1.499999999999999778 ) ;
#15408=ORIENTED_EDGE ( 'NONE', *, *, #5101, .F. ) ;
#15941=ORIENTED_EDGE ( 'NONE', *, *, #7856, .T. ) ;
#16053=AXIS2_PLACEMENT_3D ( 'NONE', #11493, #19333, #17280 ) ;
#16231=FILL_AREA_STYLE ('',( #17574 ) ) ;
#16605=SURFACE_STYLE_FILL_AREA ( #9024 ) ;
#16835=DIRECTION ( 'NONE',  ( 0.000000000000000000, 0.9992330079037401447, -0.03915859951075795903 ) ) ;
#16873=SURFACE_STYLE_USAGE ( .BOTH. , #11209 ) ;
#17230=MECHANICAL_DESIGN_GEOMETRIC_PRESENTATION_REPRESENTATION('',(#20939),#21339);
#17280=DIRECTION ( 'NONE',  ( 0.000000000000000000, 0.9992330079037401447, -0.03915859951075795903 ) ) ;
#17574=FILL_AREA_STYLE_COLOUR ( '', #3230 ) ;
#17629=ADVANCED_FACE ( 'NONE', ( #22670 ), #883, .T. ) ;
#17663=PRODUCT_DEFINITION ( 'UNKNOWN', '', #6371, #14393 ) ;
#17843=EDGE_CURVE ( 'NONE', #5671, #23981, #13259, .T. ) ;
#18261=EDGE_CURVE ( 'NONE', #5671, #4880, #7060, .T. ) ;
#18298=ORIENTED_EDGE ( 'NONE', *, *, #17843, .F. ) ;
#18493=DIRECTION ( 'NONE',  ( 0.000000000000000000, 0.9992330079037401447, -0.03915859951076000600 ) ) ;
#18556=DIRECTION ( 'NONE',  ( 0.000000000000000000, -0.9992330079037401447, 0.03915859951075795903 ) ) ;
#18745=PLANE ( 'NONE',  #6114 ) ;
#18818=CLOSED_SHELL ( 'NONE', ( #9135, #25236, #7395, #17629 ) ) ;
#18869=ORIENTED_EDGE ( 'NONE', *, *, #10136, .T. ) ;
#18914=DIRECTION ( 'NONE',  ( -1.000000000000000000, 0.000000000000000000, 0.000000000000000000 ) ) ;
#18933=( NAMED_UNIT ( * ) PLANE_ANGLE_UNIT ( ) SI_UNIT ( $, .RADIAN. ) );
#19333=DIRECTION ( 'NONE',  ( 1.000000000000000000, 0.000000000000000000, 0.000000000000000000 ) ) ;
#19352=SHAPE_DEFINITION_REPRESENTATION ( #13630, #4169 ) ;
#19657=CARTESIAN_POINT ( 'NONE',  ( 47.84183937708599643, -33.05991196579839198, 70.24627502810386659 ) ) ;
#19778=ORIENTED_EDGE ( 'NONE', *, *, #10136, .F. ) ;
#19873=AXIS2_PLACEMENT_3D ( 'NONE', #21986, #4213, #22106 ) ;
#20224=SURFACE_STYLE_USAGE ( .BOTH. , #13831 ) ;
#20617=CARTESIAN_POINT ( 'NONE',  ( 47.84183937708599643, -34.55876147765400219, 70.30501292737000085 ) ) ;
#20816=DIRECTION ( 'NONE',  ( -1.000000000000000000, 0.000000000000000000, 0.000000000000000000 ) ) ;
#20868=DIRECTION ( 'NONE',  ( -1.000000000000000000, 0.000000000000000000, 0.000000000000000000 ) ) ;
#20939=STYLED_ITEM ( 'NONE', ( #9847 ), #25444 ) ;
#21167=PRODUCT_CONTEXT ( 'NONE', #24577, 'mechanical' ) ;
#21339=( GEOMETRIC_REPRESENTATION_CONTEXT ( 3 ) GLOBAL_UNCERTAINTY_ASSIGNED_CONTEXT ( ( #24129 ) ) GLOBAL_UNIT_ASSIGNED_CONTEXT ( ( #12385, #14428, #4639 ) ) REPRESENTATION_CONTEXT ( 'NONE', 'WORKASPACE' ) );
#21986=CARTESIAN_POINT ( 'NONE',  ( 28.84183937708599998, -34.55876147765400219, 70.30501292737000085 ) ) ;
#22039=DIRECTION ( 'NONE',  ( 1.000000000000000000, 0.000000000000000000, 0.000000000000000000 ) ) ;
#22106=DIRECTION ( 'NONE',  ( 0.000000000000000000, 0.9992330079037401447, -0.03915859951075795903 ) ) ;
#22187=ORIENTED_EDGE ( 'NONE', *, *, #18261, .T. ) ;
#22296=CIRCLE ( 'NONE', #25148, 1.499999999999999778 ) ;
#22499=DIRECTION ( 'NONE',  ( 1.000000000000000000, 0.000000000000000000, 0.000000000000000000 ) ) ;
#22537=DIRECTION ( 'NONE',  ( 1.000000000000000000, 0.000000000000000000, 0.000000000000000000 ) ) ;
#22670=FACE_OUTER_BOUND ( 'NONE', #1012, .T. ) ;
#22792=PRESENTATION_STYLE_ASSIGNMENT (( #16873 ) ) ;
#22885=VERTEX_POINT ( 'NONE', #969 ) ;
#22889=DIRECTION ( 'NONE',  ( 0.000000000000000000, -0.9992330079037401447, 0.03915859951075795903 ) ) ;
#23253=ORIENTED_EDGE ( 'NONE', *, *, #10334, .T. ) ;
#23486=ORIENTED_EDGE ( 'NONE', *, *, #7856, .F. ) ;
#23697=PRODUCT ( 'Base Pivot Pin', 'Base Pivot Pin', '', ( #21167 ) ) ;
#23981=VERTEX_POINT ( 'NONE', #1128 ) ;
#24129=UNCERTAINTY_MEASURE_WITH_UNIT (LENGTH_MEASURE( 1.000000000000000082E-05 ), #12385, 'distance_accuracy_value', 'NONE');
#24138=DIRECTION ( 'NONE',  ( 1.000000000000000000, 0.000000000000000000, 0.000000000000000000 ) ) ;
#24188=UNCERTAINTY_MEASURE_WITH_UNIT (LENGTH_MEASURE( 1.000000000000000082E-05 ), #11078, 'distance_accuracy_value', 'NONE');
#24374=CIRCLE ( 'NONE', #19873, 1.499999999999999778 ) ;
#24577=APPLICATION_CONTEXT ( 'automotive_design' ) ;
#24808=CARTESIAN_POINT ( 'NONE',  ( 47.84183937708599643, -34.55876147765400219, 70.30501292737000085 ) ) ;
#24948=( NAMED_UNIT ( * ) SI_UNIT ( $, .STERADIAN. ) SOLID_ANGLE_UNIT ( ) );
#25148=AXIS2_PLACEMENT_3D ( 'NONE', #3617, #13802, #6 ) ;
#25236=ADVANCED_FACE ( 'NONE', ( #5094 ), #18745, .T. ) ;
#25444=MANIFOLD_SOLID_BREP ( 'NONE', #18818 ) ;
ENDSEC;
END-ISO-10303-21;
